ISO-10303-21;
HEADER;
/* Generated by software containing ST-Developer
 * from STEP Tools, Inc. (www.steptools.com) 
 */

FILE_DESCRIPTION(
/* description */ ('CAx-IF Rec.Pracs.---Representation and Presentation of Product Manufa
cturing Information (PMI)---4.0---2014-10-13'),
/* implementation_level */ '2;1');

FILE_NAME(
/* name */ 'Washer.step',
/* time_stamp */ '2026-10-24T16:53:48-07:00',
/* author */ (''),
/* organization */ (''),
/* preprocessor_version */ 'ST-DEVELOPER v20.2',
/* originating_system */ 'Autodesk Translation Framework v15.17.0.0',
/* authorisation */ '');

FILE_SCHEMA (('AP242_MANAGED_MODEL_BASED_3D_ENGINEERING_MIM_LF { 1 0 10303 442 2 1 4 }'));
ENDSEC;

DATA;
#10=MECHANICAL_DESIGN_GEOMETRIC_PRESENTATION_REPRESENTATION('',(#3489),#107910);
#3469=SHAPE_REPRESENTATION_RELATIONSHIP('SRR','None',#107947,#3479);
#3479=ADVANCED_BREP_SHAPE_REPRESENTATION('',(#3499),#107900);
#3489=STYLED_ITEM('',(#108006),#3499);
#3499=MANIFOLD_SOLID_BREP('Body1',#45537);
#3509=FACE_BOUND('',#6685,.T.);
#3510=FACE_BOUND('',#6687,.T.);
#3542=PLANE('',#45666);
#3543=PLANE('',#45667);
#3758=FACE_OUTER_BOUND('',#6682,.T.);
#3759=FACE_OUTER_BOUND('',#6683,.T.);
#3760=FACE_OUTER_BOUND('',#6684,.T.);
#3761=FACE_OUTER_BOUND('',#6686,.T.);
#6682=EDGE_LOOP('',(#28122,#28123,#28124,#28125));
#6683=EDGE_LOOP('',(#28126,#28127,#28128,#28129));
#6684=EDGE_LOOP('',(#28130));
#6685=EDGE_LOOP('',(#28131));
#6686=EDGE_LOOP('',(#28132));
#6687=EDGE_LOOP('',(#28133));
#9639=LINE('',#61802,#11623);
#9640=LINE('',#61808,#11624);
#11623=VECTOR('',#50384,0.0015);
#11624=VECTOR('',#50391,0.004);
#13607=CIRCLE('',#45661,0.00150000000001001);
#13608=CIRCLE('',#45662,0.00150000000001001);
#13609=CIRCLE('',#45664,0.00400000000001001);
#13610=CIRCLE('',#45665,0.00400000000001001);
#17179=VERTEX_POINT('',#61799);
#17180=VERTEX_POINT('',#61801);
#17181=VERTEX_POINT('',#61805);
#17182=VERTEX_POINT('',#61807);
#21203=EDGE_CURVE('',#17179,#17179,#13607,.T.);
#21204=EDGE_CURVE('',#17179,#17180,#9639,.T.);
#21205=EDGE_CURVE('',#17180,#17180,#13608,.T.);
#21206=EDGE_CURVE('',#17181,#17181,#13609,.T.);
#21207=EDGE_CURVE('',#17181,#17182,#9640,.T.);
#21208=EDGE_CURVE('',#17182,#17182,#13610,.T.);
#28122=ORIENTED_EDGE('',*,*,#21203,.T.);
#28123=ORIENTED_EDGE('',*,*,#21204,.T.);
#28124=ORIENTED_EDGE('',*,*,#21205,.F.);
#28125=ORIENTED_EDGE('',*,*,#21204,.F.);
#28126=ORIENTED_EDGE('',*,*,#21206,.T.);
#28127=ORIENTED_EDGE('',*,*,#21207,.T.);
#28128=ORIENTED_EDGE('',*,*,#21208,.F.);
#28129=ORIENTED_EDGE('',*,*,#21207,.F.);
#28130=ORIENTED_EDGE('',*,*,#21208,.T.);
#28131=ORIENTED_EDGE('',*,*,#21203,.F.);
#28132=ORIENTED_EDGE('',*,*,#21206,.F.);
#28133=ORIENTED_EDGE('',*,*,#21205,.T.);
#41960=CYLINDRICAL_SURFACE('',#45660,0.0015);
#41961=CYLINDRICAL_SURFACE('',#45663,0.004);
#42613=ADVANCED_FACE('',(#3758),#41960,.F.);
#42614=ADVANCED_FACE('',(#3759),#41961,.T.);
#42615=ADVANCED_FACE('',(#3760,#3509),#3542,.T.);
#42616=ADVANCED_FACE('',(#3761,#3510),#3543,.F.);
#45537=CLOSED_SHELL('',(#42613,#42614,#42615,#42616));
#45659=AXIS2_PLACEMENT_3D('',#61797,#50378,#50379);
#45660=AXIS2_PLACEMENT_3D('',#61798,#50380,#50381);
#45661=AXIS2_PLACEMENT_3D('',#61800,#50382,#50383);
#45662=AXIS2_PLACEMENT_3D('',#61803,#50385,#50386);
#45663=AXIS2_PLACEMENT_3D('',#61804,#50387,#50388);
#45664=AXIS2_PLACEMENT_3D('',#61806,#50389,#50390);
#45665=AXIS2_PLACEMENT_3D('',#61809,#50392,#50393);
#45666=AXIS2_PLACEMENT_3D('',#61810,#50394,#50395);
#45667=AXIS2_PLACEMENT_3D('',#61811,#50396,#50397);
#50378=DIRECTION('axis',(0.,0.,1.));
#50379=DIRECTION('refdir',(1.,0.,0.));
#50380=DIRECTION('center_axis',(0.,1.,-1.45983193964168E-32));
#50381=DIRECTION('ref_axis',(-1.,0.,0.));
#50382=DIRECTION('center_axis',(0.,-1.,6.6666666666222E-12));
#50383=DIRECTION('ref_axis',(1.,0.,0.));
#50384=DIRECTION('',(0.,1.,-1.45983193964168E-32));
#50385=DIRECTION('center_axis',(0.,-1.,6.6666666666222E-12));
#50386=DIRECTION('ref_axis',(1.,0.,0.));
#50387=DIRECTION('center_axis',(0.,1.,-1.45983193964168E-32));
#50388=DIRECTION('ref_axis',(-1.,0.,0.));
#50389=DIRECTION('center_axis',(0.,-1.,2.49999999999375E-12));
#50390=DIRECTION('ref_axis',(1.,0.,0.));
#50391=DIRECTION('',(0.,-1.,1.45983193964168E-32));
#50392=DIRECTION('center_axis',(0.,-1.,2.49999999999375E-12));
#50393=DIRECTION('ref_axis',(1.,0.,0.));
#50394=DIRECTION('center_axis',(-1.19900741137893E-16,-1.,1.45983193964168E-32));
#50395=DIRECTION('ref_axis',(-1.,1.19900741137893E-16,0.));
#50396=DIRECTION('center_axis',(-1.19900741137893E-16,-1.,1.45983193964168E-32));
#50397=DIRECTION('ref_axis',(-1.,1.19900741137893E-16,0.));
#61797=CARTESIAN_POINT('',(0.,0.,0.));
#61798=CARTESIAN_POINT('Origin',(0.00812378219310841,-0.0211741814719619,
0.07415));
#61799=CARTESIAN_POINT('',(0.00962378219312842,-0.0211741814719719,0.07415000000001));
#61800=CARTESIAN_POINT('Origin',(0.00812378219311841,-0.0211741814719719,
0.07415000000001));
#61801=CARTESIAN_POINT('',(0.00962378219312842,-0.0201741814719718,0.07415000000001));
#61802=CARTESIAN_POINT('',(0.00962378219310841,-0.0211741814719619,0.07415));
#61803=CARTESIAN_POINT('Origin',(0.00812378219311841,-0.0201741814719718,
0.07415000000001));
#61804=CARTESIAN_POINT('Origin',(0.00812378219310841,-0.0211741814719619,
0.07415));
#61805=CARTESIAN_POINT('',(0.0121237821931284,-0.0201741814719718,0.07415000000001));
#61806=CARTESIAN_POINT('Origin',(0.00812378219311841,-0.0201741814719718,
0.07415000000001));
#61807=CARTESIAN_POINT('',(0.0121237821931284,-0.0211741814719719,0.07415000000001));
#61808=CARTESIAN_POINT('',(0.0121237821931084,-0.0211741814719619,0.07415));
#61809=CARTESIAN_POINT('Origin',(0.00812378219311841,-0.0211741814719719,
0.07415000000001));
#61810=CARTESIAN_POINT('Origin',(0.00812378219310841,-0.0211741814719619,
0.07415));
#61811=CARTESIAN_POINT('Origin',(0.00812378219310841,-0.0201741814719619,
0.07415));
#107888=UNCERTAINTY_MEASURE_WITH_UNIT(LENGTH_MEASURE(1.E-5),#107911,
'DISTANCE_ACCURACY_VALUE',
'Maximum model space distance between geometric entities at asserted c
onnectivities');
#107898=UNCERTAINTY_MEASURE_WITH_UNIT(LENGTH_MEASURE(1.E-5),#107911,
'DISTANCE_ACCURACY_VALUE',
'Maximum model space distance between geometric entities at asserted c
onnectivities');
#107900=(
GEOMETRIC_REPRESENTATION_CONTEXT(3)
GLOBAL_UNCERTAINTY_ASSIGNED_CONTEXT((#107888))
GLOBAL_UNIT_ASSIGNED_CONTEXT((#107911,#107912,#107913))
REPRESENTATION_CONTEXT('','3D')
);
#107910=(
GEOMETRIC_REPRESENTATION_CONTEXT(3)
GLOBAL_UNCERTAINTY_ASSIGNED_CONTEXT((#107898))
GLOBAL_UNIT_ASSIGNED_CONTEXT((#107911,#107912,#107913))
REPRESENTATION_CONTEXT('','3D')
);
#107911=(
LENGTH_UNIT()
NAMED_UNIT(*)
SI_UNIT($,.METRE.)
);
#107912=(
NAMED_UNIT(*)
PLANE_ANGLE_UNIT()
SI_UNIT($,.RADIAN.)
);
#107913=(
NAMED_UNIT(*)
SI_UNIT($,.STERADIAN.)
SOLID_ANGLE_UNIT()
);
#107915=SHAPE_DEFINITION_REPRESENTATION(#107926,#107947);
#107926=PRODUCT_DEFINITION_SHAPE('',$,#107959);
#107947=SHAPE_REPRESENTATION('',(#45659),#107900);
#107957=PRODUCT_DEFINITION_CONTEXT('part definition',#107992,'design');
#107959=PRODUCT_DEFINITION('Washer','Washer',#107970,#107957);
#107970=PRODUCT_DEFINITION_FORMATION('',$,#107995);
#107992=APPLICATION_CONTEXT('Managed model based 3d engineering');
#107993=PRODUCT_CONTEXT('part definition',#107992,'mechanical');
#107995=PRODUCT('Washer','Washer',
'LEGAL AND USAGE DISCLAIMER: this Data/Model is provided \X2\201C\X0\A
S IS\X2\201D\X0\ for informational and representational only. It is a 
geometric approximation and is NOT engineered, certified, or guarantee
d for dimensional accuracy, exact tolerances, or production-level prec
ision. Vendor disclaims all implied warranties including fitness for a
 particular purpose. DO NOT USE FOR DIRECT PHYSICAL MANUFACTURING, AUT
OMATED PRODUCTION, OR SAFETY-CRITICAL SYSTEMS without independent engi
neering verification and resolution of any design discrepancies.',(#107993));
#108006=PRESENTATION_STYLE_ASSIGNMENT((#108013));
#108013=SURFACE_STYLE_USAGE(.BOTH.,#108020);
#108020=SURFACE_SIDE_STYLE('',(#108027));
#108027=SURFACE_STYLE_FILL_AREA(#108034);
#108034=FILL_AREA_STYLE('Opaque(25,25,25)',(#108041));
#108041=FILL_AREA_STYLE_COLOUR('Opaque(25,25,25)',#108048);
#108048=COLOUR_RGB('Opaque(25,25,25)',0.0980392156862745,0.0980392156862745,
0.0980392156862745);
ENDSEC;
END-ISO-10303-21;
